ISO-10303-21;
HEADER;
/* Generated by software containing ST-Developer
 * from STEP Tools, Inc. (www.steptools.com) 
 */

FILE_DESCRIPTION(
/* description */ ('Single-Axis Profile-Rail Linear Slide'),
/* implementation_level */ '2;1');

FILE_NAME(
/* name */ 'Cap Screw - M4x16.step',
/* time_stamp */ '2026-10-27T10:47:43-07:00',
/* author */ (''),
/* organization */ (''),
/* preprocessor_version */ 'ST-DEVELOPER v20.2',
/* originating_system */ 'Autodesk Translation Framework v15.17.0.0',
/* authorisation */ '');

FILE_SCHEMA (('AUTOMOTIVE_DESIGN { 1 0 10303 214 3 1 1 }'));
ENDSEC;

DATA;
#10=MECHANICAL_DESIGN_GEOMETRIC_PRESENTATION_REPRESENTATION('',(#353),#14478);
#255=CONICAL_SURFACE('',#9508,0.325,0.785398163397448);
#256=CONICAL_SURFACE('',#9512,0.335,0.785398163397448);
#257=CONICAL_SURFACE('',#9516,0.21,0.463647609000806);
#258=CONICAL_SURFACE('',#9520,0.18,0.785398163397448);
#266=ORIENTED_CLOSED_SHELL('',*,#8617,.F.);
#271=BREP_WITH_VOIDS('Body1',#8616,(#266));
#299=SHAPE_REPRESENTATION_RELATIONSHIP('SRR','None',#14631,#326);
#326=ADVANCED_BREP_SHAPE_REPRESENTATION('',(#271),#14475);
#353=STYLED_ITEM('',(#14838),#271);
#464=FACE_BOUND('',#1803,.T.);
#816=PLANE('',#9506);
#817=PLANE('',#9514);
#818=PLANE('',#9522);
#819=PLANE('',#9523);
#820=PLANE('',#9524);
#821=PLANE('',#9525);
#822=PLANE('',#9526);
#823=PLANE('',#9527);
#824=PLANE('',#9528);
#825=PLANE('',#9529);
#826=PLANE('',#9530);
#1257=FACE_OUTER_BOUND('',#1798,.T.);
#1258=FACE_OUTER_BOUND('',#1799,.T.);
#1259=FACE_OUTER_BOUND('',#1800,.T.);
#1260=FACE_OUTER_BOUND('',#1801,.T.);
#1261=FACE_OUTER_BOUND('',#1802,.T.);
#1262=FACE_OUTER_BOUND('',#1804,.T.);
#1263=FACE_OUTER_BOUND('',#1805,.T.);
#1264=FACE_OUTER_BOUND('',#1806,.T.);
#1265=FACE_OUTER_BOUND('',#1807,.T.);
#1266=FACE_OUTER_BOUND('',#1808,.T.);
#1267=FACE_OUTER_BOUND('',#1809,.T.);
#1268=FACE_OUTER_BOUND('',#1810,.T.);
#1269=FACE_OUTER_BOUND('',#1811,.T.);
#1270=FACE_OUTER_BOUND('',#1812,.T.);
#1271=FACE_OUTER_BOUND('',#1813,.T.);
#1272=FACE_OUTER_BOUND('',#1814,.T.);
#1273=FACE_OUTER_BOUND('',#1815,.T.);
#1798=EDGE_LOOP('',(#7931));
#1799=EDGE_LOOP('',(#7932,#7933,#7934,#7935));
#1800=EDGE_LOOP('',(#7936,#7937,#7938,#7939));
#1801=EDGE_LOOP('',(#7940,#7941,#7942,#7943));
#1802=EDGE_LOOP('',(#7944));
#1803=EDGE_LOOP('',(#7945));
#1804=EDGE_LOOP('',(#7946,#7947,#7948,#7949));
#1805=EDGE_LOOP('',(#7950,#7951,#7952,#7953));
#1806=EDGE_LOOP('',(#7954,#7955,#7956,#7957));
#1807=EDGE_LOOP('',(#7958));
#1808=EDGE_LOOP('',(#7959,#7960,#7961,#7962));
#1809=EDGE_LOOP('',(#7963,#7964,#7965,#7966));
#1810=EDGE_LOOP('',(#7967,#7968,#7969,#7970));
#1811=EDGE_LOOP('',(#7971,#7972,#7973,#7974));
#1812=EDGE_LOOP('',(#7975,#7976,#7977,#7978));
#1813=EDGE_LOOP('',(#7979,#7980,#7981,#7982));
#1814=EDGE_LOOP('',(#7983,#7984,#7985,#7986,#7987,#7988));
#1815=EDGE_LOOP('',(#7989,#7990,#7991,#7992,#7993,#7994));
#2761=LINE('',#14212,#3732);
#2762=LINE('',#14216,#3733);
#2763=LINE('',#14220,#3734);
#2764=LINE('',#14227,#3735);
#2765=LINE('',#14231,#3736);
#2766=LINE('',#14235,#3737);
#2767=LINE('',#14240,#3738);
#2768=LINE('',#14242,#3739);
#2769=LINE('',#14244,#3740);
#2770=LINE('',#14245,#3741);
#2771=LINE('',#14248,#3742);
#2772=LINE('',#14250,#3743);
#2773=LINE('',#14251,#3744);
#2774=LINE('',#14254,#3745);
#2775=LINE('',#14256,#3746);
#2776=LINE('',#14257,#3747);
#2777=LINE('',#14260,#3748);
#2778=LINE('',#14262,#3749);
#2779=LINE('',#14263,#3750);
#2780=LINE('',#14266,#3751);
#2781=LINE('',#14268,#3752);
#2782=LINE('',#14269,#3753);
#2783=LINE('',#14271,#3754);
#2784=LINE('',#14272,#3755);
#3732=VECTOR('',#11724,0.325);
#3733=VECTOR('',#11729,0.35);
#3734=VECTOR('',#11734,0.335);
#3735=VECTOR('',#11743,0.21);
#3736=VECTOR('',#11748,0.2);
#3737=VECTOR('',#11753,0.18);
#3738=VECTOR('',#11758,1.);
#3739=VECTOR('',#11759,1.);
#3740=VECTOR('',#11760,1.);
#3741=VECTOR('',#11761,1.);
#3742=VECTOR('',#11764,1.);
#3743=VECTOR('',#11765,1.);
#3744=VECTOR('',#11766,1.);
#3745=VECTOR('',#11769,1.);
#3746=VECTOR('',#11770,1.);
#3747=VECTOR('',#11771,1.);
#3748=VECTOR('',#11774,1.);
#3749=VECTOR('',#11775,1.);
#3750=VECTOR('',#11776,1.);
#3751=VECTOR('',#11779,1.);
#3752=VECTOR('',#11780,1.);
#3753=VECTOR('',#11781,1.);
#3754=VECTOR('',#11784,1.);
#3755=VECTOR('',#11785,1.);
#3918=CIRCLE('',#9507,0.3);
#3919=CIRCLE('',#9509,0.35);
#3920=CIRCLE('',#9511,0.35);
#3921=CIRCLE('',#9513,0.32);
#3922=CIRCLE('',#9515,0.22);
#3923=CIRCLE('',#9517,0.1954);
#3924=CIRCLE('',#9519,0.1954);
#3925=CIRCLE('',#9521,0.16);
#4640=VERTEX_POINT('',#14207);
#4641=VERTEX_POINT('',#14210);
#4642=VERTEX_POINT('',#14214);
#4643=VERTEX_POINT('',#14218);
#4644=VERTEX_POINT('',#14222);
#4645=VERTEX_POINT('',#14225);
#4646=VERTEX_POINT('',#14229);
#4647=VERTEX_POINT('',#14233);
#4648=VERTEX_POINT('',#14238);
#4649=VERTEX_POINT('',#14239);
#4650=VERTEX_POINT('',#14241);
#4651=VERTEX_POINT('',#14243);
#4652=VERTEX_POINT('',#14247);
#4653=VERTEX_POINT('',#14249);
#4654=VERTEX_POINT('',#14253);
#4655=VERTEX_POINT('',#14255);
#4656=VERTEX_POINT('',#14259);
#4657=VERTEX_POINT('',#14261);
#4658=VERTEX_POINT('',#14265);
#4659=VERTEX_POINT('',#14267);
#5743=EDGE_CURVE('',#4640,#4640,#3918,.T.);
#5744=EDGE_CURVE('',#4641,#4641,#3919,.T.);
#5745=EDGE_CURVE('',#4641,#4640,#2761,.T.);
#5746=EDGE_CURVE('',#4642,#4642,#3920,.T.);
#5747=EDGE_CURVE('',#4642,#4641,#2762,.T.);
#5748=EDGE_CURVE('',#4643,#4643,#3921,.T.);
#5749=EDGE_CURVE('',#4643,#4642,#2763,.T.);
#5750=EDGE_CURVE('',#4644,#4644,#3922,.T.);
#5751=EDGE_CURVE('',#4645,#4645,#3923,.F.);
#5752=EDGE_CURVE('',#4645,#4644,#2764,.T.);
#5753=EDGE_CURVE('',#4646,#4646,#3924,.F.);
#5754=EDGE_CURVE('',#4646,#4645,#2765,.T.);
#5755=EDGE_CURVE('',#4647,#4647,#3925,.T.);
#5756=EDGE_CURVE('',#4647,#4646,#2766,.T.);
#5757=EDGE_CURVE('',#4648,#4649,#2767,.T.);
#5758=EDGE_CURVE('',#4649,#4650,#2768,.T.);
#5759=EDGE_CURVE('',#4650,#4651,#2769,.T.);
#5760=EDGE_CURVE('',#4648,#4651,#2770,.T.);
#5761=EDGE_CURVE('',#4649,#4652,#2771,.T.);
#5762=EDGE_CURVE('',#4652,#4653,#2772,.T.);
#5763=EDGE_CURVE('',#4653,#4650,#2773,.T.);
#5764=EDGE_CURVE('',#4652,#4654,#2774,.T.);
#5765=EDGE_CURVE('',#4654,#4655,#2775,.T.);
#5766=EDGE_CURVE('',#4655,#4653,#2776,.T.);
#5767=EDGE_CURVE('',#4654,#4656,#2777,.T.);
#5768=EDGE_CURVE('',#4656,#4657,#2778,.T.);
#5769=EDGE_CURVE('',#4657,#4655,#2779,.T.);
#5770=EDGE_CURVE('',#4656,#4658,#2780,.T.);
#5771=EDGE_CURVE('',#4658,#4659,#2781,.T.);
#5772=EDGE_CURVE('',#4659,#4657,#2782,.T.);
#5773=EDGE_CURVE('',#4658,#4648,#2783,.T.);
#5774=EDGE_CURVE('',#4651,#4659,#2784,.T.);
#7931=ORIENTED_EDGE('',*,*,#5743,.F.);
#7932=ORIENTED_EDGE('',*,*,#5744,.F.);
#7933=ORIENTED_EDGE('',*,*,#5745,.T.);
#7934=ORIENTED_EDGE('',*,*,#5743,.T.);
#7935=ORIENTED_EDGE('',*,*,#5745,.F.);
#7936=ORIENTED_EDGE('',*,*,#5746,.F.);
#7937=ORIENTED_EDGE('',*,*,#5747,.T.);
#7938=ORIENTED_EDGE('',*,*,#5744,.T.);
#7939=ORIENTED_EDGE('',*,*,#5747,.F.);
#7940=ORIENTED_EDGE('',*,*,#5748,.F.);
#7941=ORIENTED_EDGE('',*,*,#5749,.T.);
#7942=ORIENTED_EDGE('',*,*,#5746,.T.);
#7943=ORIENTED_EDGE('',*,*,#5749,.F.);
#7944=ORIENTED_EDGE('',*,*,#5748,.T.);
#7945=ORIENTED_EDGE('',*,*,#5750,.F.);
#7946=ORIENTED_EDGE('',*,*,#5751,.F.);
#7947=ORIENTED_EDGE('',*,*,#5752,.T.);
#7948=ORIENTED_EDGE('',*,*,#5750,.T.);
#7949=ORIENTED_EDGE('',*,*,#5752,.F.);
#7950=ORIENTED_EDGE('',*,*,#5753,.F.);
#7951=ORIENTED_EDGE('',*,*,#5754,.T.);
#7952=ORIENTED_EDGE('',*,*,#5751,.T.);
#7953=ORIENTED_EDGE('',*,*,#5754,.F.);
#7954=ORIENTED_EDGE('',*,*,#5755,.F.);
#7955=ORIENTED_EDGE('',*,*,#5756,.T.);
#7956=ORIENTED_EDGE('',*,*,#5753,.T.);
#7957=ORIENTED_EDGE('',*,*,#5756,.F.);
#7958=ORIENTED_EDGE('',*,*,#5755,.T.);
#7959=ORIENTED_EDGE('',*,*,#5757,.T.);
#7960=ORIENTED_EDGE('',*,*,#5758,.T.);
#7961=ORIENTED_EDGE('',*,*,#5759,.T.);
#7962=ORIENTED_EDGE('',*,*,#5760,.F.);
#7963=ORIENTED_EDGE('',*,*,#5761,.T.);
#7964=ORIENTED_EDGE('',*,*,#5762,.T.);
#7965=ORIENTED_EDGE('',*,*,#5763,.T.);
#7966=ORIENTED_EDGE('',*,*,#5758,.F.);
#7967=ORIENTED_EDGE('',*,*,#5764,.T.);
#7968=ORIENTED_EDGE('',*,*,#5765,.T.);
#7969=ORIENTED_EDGE('',*,*,#5766,.T.);
#7970=ORIENTED_EDGE('',*,*,#5762,.F.);
#7971=ORIENTED_EDGE('',*,*,#5767,.T.);
#7972=ORIENTED_EDGE('',*,*,#5768,.T.);
#7973=ORIENTED_EDGE('',*,*,#5769,.T.);
#7974=ORIENTED_EDGE('',*,*,#5765,.F.);
#7975=ORIENTED_EDGE('',*,*,#5770,.T.);
#7976=ORIENTED_EDGE('',*,*,#5771,.T.);
#7977=ORIENTED_EDGE('',*,*,#5772,.T.);
#7978=ORIENTED_EDGE('',*,*,#5768,.F.);
#7979=ORIENTED_EDGE('',*,*,#5773,.T.);
#7980=ORIENTED_EDGE('',*,*,#5760,.T.);
#7981=ORIENTED_EDGE('',*,*,#5774,.T.);
#7982=ORIENTED_EDGE('',*,*,#5771,.F.);
#7983=ORIENTED_EDGE('',*,*,#5773,.F.);
#7984=ORIENTED_EDGE('',*,*,#5770,.F.);
#7985=ORIENTED_EDGE('',*,*,#5767,.F.);
#7986=ORIENTED_EDGE('',*,*,#5764,.F.);
#7987=ORIENTED_EDGE('',*,*,#5761,.F.);
#7988=ORIENTED_EDGE('',*,*,#5757,.F.);
#7989=ORIENTED_EDGE('',*,*,#5774,.F.);
#7990=ORIENTED_EDGE('',*,*,#5759,.F.);
#7991=ORIENTED_EDGE('',*,*,#5763,.F.);
#7992=ORIENTED_EDGE('',*,*,#5766,.F.);
#7993=ORIENTED_EDGE('',*,*,#5769,.F.);
#7994=ORIENTED_EDGE('',*,*,#5772,.F.);
#8128=CYLINDRICAL_SURFACE('',#9510,0.35);
#8129=CYLINDRICAL_SURFACE('',#9518,0.1954);
#8551=ADVANCED_FACE('',(#1257),#816,.T.);
#8552=ADVANCED_FACE('',(#1258),#255,.T.);
#8553=ADVANCED_FACE('',(#1259),#8128,.T.);
#8554=ADVANCED_FACE('',(#1260),#256,.T.);
#8555=ADVANCED_FACE('',(#1261,#464),#817,.T.);
#8556=ADVANCED_FACE('',(#1262),#257,.T.);
#8557=ADVANCED_FACE('',(#1263),#8129,.T.);
#8558=ADVANCED_FACE('',(#1264),#258,.T.);
#8559=ADVANCED_FACE('',(#1265),#818,.T.);
#8560=ADVANCED_FACE('',(#1266),#819,.F.);
#8561=ADVANCED_FACE('',(#1267),#820,.F.);
#8562=ADVANCED_FACE('',(#1268),#821,.F.);
#8563=ADVANCED_FACE('',(#1269),#822,.F.);
#8564=ADVANCED_FACE('',(#1270),#823,.F.);
#8565=ADVANCED_FACE('',(#1271),#824,.F.);
#8566=ADVANCED_FACE('',(#1272),#825,.F.);
#8567=ADVANCED_FACE('',(#1273),#826,.F.);
#8616=CLOSED_SHELL('',(#8551,#8552,#8553,#8554,#8555,#8556,#8557,#8558,
#8559));
#8617=CLOSED_SHELL('',(#8560,#8561,#8562,#8563,#8564,#8565,#8566,#8567));
#9505=AXIS2_PLACEMENT_3D('',#14205,#11714,#11715);
#9506=AXIS2_PLACEMENT_3D('',#14206,#11716,#11717);
#9507=AXIS2_PLACEMENT_3D('',#14208,#11718,#11719);
#9508=AXIS2_PLACEMENT_3D('',#14209,#11720,#11721);
#9509=AXIS2_PLACEMENT_3D('',#14211,#11722,#11723);
#9510=AXIS2_PLACEMENT_3D('',#14213,#11725,#11726);
#9511=AXIS2_PLACEMENT_3D('',#14215,#11727,#11728);
#9512=AXIS2_PLACEMENT_3D('',#14217,#11730,#11731);
#9513=AXIS2_PLACEMENT_3D('',#14219,#11732,#11733);
#9514=AXIS2_PLACEMENT_3D('',#14221,#11735,#11736);
#9515=AXIS2_PLACEMENT_3D('',#14223,#11737,#11738);
#9516=AXIS2_PLACEMENT_3D('',#14224,#11739,#11740);
#9517=AXIS2_PLACEMENT_3D('',#14226,#11741,#11742);
#9518=AXIS2_PLACEMENT_3D('',#14228,#11744,#11745);
#9519=AXIS2_PLACEMENT_3D('',#14230,#11746,#11747);
#9520=AXIS2_PLACEMENT_3D('',#14232,#11749,#11750);
#9521=AXIS2_PLACEMENT_3D('',#14234,#11751,#11752);
#9522=AXIS2_PLACEMENT_3D('',#14236,#11754,#11755);
#9523=AXIS2_PLACEMENT_3D('',#14237,#11756,#11757);
#9524=AXIS2_PLACEMENT_3D('',#14246,#11762,#11763);
#9525=AXIS2_PLACEMENT_3D('',#14252,#11767,#11768);
#9526=AXIS2_PLACEMENT_3D('',#14258,#11772,#11773);
#9527=AXIS2_PLACEMENT_3D('',#14264,#11777,#11778);
#9528=AXIS2_PLACEMENT_3D('',#14270,#11782,#11783);
#9529=AXIS2_PLACEMENT_3D('',#14273,#11786,#11787);
#9530=AXIS2_PLACEMENT_3D('',#14274,#11788,#11789);
#11714=DIRECTION('axis',(0.,0.,1.));
#11715=DIRECTION('refdir',(1.,0.,0.));
#11716=DIRECTION('center_axis',(0.,1.,0.));
#11717=DIRECTION('ref_axis',(0.,0.,1.));
#11718=DIRECTION('center_axis',(0.,-1.,0.));
#11719=DIRECTION('ref_axis',(1.,0.,0.));
#11720=DIRECTION('center_axis',(0.,-1.,0.));
#11721=DIRECTION('ref_axis',(1.,0.,0.));
#11722=DIRECTION('center_axis',(0.,-1.,0.));
#11723=DIRECTION('ref_axis',(1.,0.,0.));
#11724=DIRECTION('',(0.707106781186547,0.707106781186548,8.65956056235493E-17));
#11725=DIRECTION('center_axis',(0.,-1.,0.));
#11726=DIRECTION('ref_axis',(1.,0.,0.));
#11727=DIRECTION('center_axis',(0.,-1.,0.));
#11728=DIRECTION('ref_axis',(1.,0.,0.));
#11729=DIRECTION('',(0.,1.,0.));
#11730=DIRECTION('center_axis',(0.,1.,0.));
#11731=DIRECTION('ref_axis',(1.,0.,0.));
#11732=DIRECTION('center_axis',(0.,-1.,0.));
#11733=DIRECTION('ref_axis',(1.,0.,0.));
#11734=DIRECTION('',(-0.707106781186547,0.707106781186548,-8.65956056235493E-17));
#11735=DIRECTION('center_axis',(0.,-1.,0.));
#11736=DIRECTION('ref_axis',(0.,0.,-1.));
#11737=DIRECTION('center_axis',(0.,-1.,0.));
#11738=DIRECTION('ref_axis',(1.,0.,0.));
#11739=DIRECTION('center_axis',(0.,1.,0.));
#11740=DIRECTION('ref_axis',(1.,0.,0.));
#11741=DIRECTION('center_axis',(0.,1.,0.));
#11742=DIRECTION('ref_axis',(1.,0.,0.));
#11743=DIRECTION('',(-0.447213595499958,0.894427190999916,-5.47678698264203E-17));
#11744=DIRECTION('center_axis',(0.,-1.,0.));
#11745=DIRECTION('ref_axis',(1.,0.,0.));
#11746=DIRECTION('center_axis',(0.,1.,0.));
#11747=DIRECTION('ref_axis',(1.,0.,0.));
#11748=DIRECTION('',(0.,1.,0.));
#11749=DIRECTION('center_axis',(0.,1.,0.));
#11750=DIRECTION('ref_axis',(1.,0.,0.));
#11751=DIRECTION('center_axis',(0.,-1.,0.));
#11752=DIRECTION('ref_axis',(1.,0.,0.));
#11753=DIRECTION('',(-0.707106781186547,0.707106781186548,-8.65956056235493E-17));
#11754=DIRECTION('center_axis',(0.,-1.,0.));
#11755=DIRECTION('ref_axis',(0.,0.,-1.));
#11756=DIRECTION('center_axis',(0.866025403784439,0.,-0.5));
#11757=DIRECTION('ref_axis',(0.5,0.,0.866025403784439));
#11758=DIRECTION('',(-0.5,0.,-0.866025403784439));
#11759=DIRECTION('',(0.,-1.,0.));
#11760=DIRECTION('',(0.5,0.,0.866025403784439));
#11761=DIRECTION('',(0.,-1.,0.));
#11762=DIRECTION('center_axis',(1.60246890531964E-16,0.,-1.));
#11763=DIRECTION('ref_axis',(1.,0.,1.60246890531964E-16));
#11764=DIRECTION('',(-1.,0.,-1.60246890531964E-16));
#11765=DIRECTION('',(0.,-1.,0.));
#11766=DIRECTION('',(1.,0.,1.60246890531964E-16));
#11767=DIRECTION('center_axis',(-0.866025403784439,0.,-0.5));
#11768=DIRECTION('ref_axis',(0.5,0.,-0.866025403784439));
#11769=DIRECTION('',(-0.5,0.,0.866025403784439));
#11770=DIRECTION('',(0.,-1.,0.));
#11771=DIRECTION('',(0.5,0.,-0.866025403784439));
#11772=DIRECTION('center_axis',(-0.866025403784439,0.,0.5));
#11773=DIRECTION('ref_axis',(-0.5,0.,-0.866025403784439));
#11774=DIRECTION('',(0.5,0.,0.866025403784439));
#11775=DIRECTION('',(0.,-1.,0.));
#11776=DIRECTION('',(-0.5,0.,-0.866025403784439));
#11777=DIRECTION('center_axis',(-1.60246890531964E-16,0.,1.));
#11778=DIRECTION('ref_axis',(-1.,0.,-1.60246890531964E-16));
#11779=DIRECTION('',(1.,0.,1.60246890531964E-16));
#11780=DIRECTION('',(0.,-1.,0.));
#11781=DIRECTION('',(-1.,0.,-1.60246890531964E-16));
#11782=DIRECTION('center_axis',(0.866025403784439,0.,0.5));
#11783=DIRECTION('ref_axis',(-0.5,0.,0.866025403784439));
#11784=DIRECTION('',(0.5,0.,-0.866025403784439));
#11785=DIRECTION('',(-0.5,0.,0.866025403784439));
#11786=DIRECTION('center_axis',(0.,1.,0.));
#11787=DIRECTION('ref_axis',(1.,0.,0.));
#11788=DIRECTION('center_axis',(0.,-1.,0.));
#11789=DIRECTION('ref_axis',(0.,0.,-1.));
#14205=CARTESIAN_POINT('',(0.,0.,0.));
#14206=CARTESIAN_POINT('Origin',(0.3,0.4,0.));
#14207=CARTESIAN_POINT('',(-0.3,0.4,-3.67394039744206E-17));
#14208=CARTESIAN_POINT('Origin',(0.,0.4,0.));
#14209=CARTESIAN_POINT('Origin',(0.,0.375,0.));
#14210=CARTESIAN_POINT('',(-0.35,0.35,-4.28626379701573E-17));
#14211=CARTESIAN_POINT('Origin',(0.,0.35,0.));
#14212=CARTESIAN_POINT('',(-0.325,0.375,-3.9801020972289E-17));
#14213=CARTESIAN_POINT('Origin',(0.,0.19,0.));
#14214=CARTESIAN_POINT('',(-0.35,0.03,-4.28626379701574E-17));
#14215=CARTESIAN_POINT('Origin',(0.,0.03,0.));
#14216=CARTESIAN_POINT('',(-0.35,0.19,-4.28626379701574E-17));
#14217=CARTESIAN_POINT('Origin',(0.,0.0149999999999999,0.));
#14218=CARTESIAN_POINT('',(-0.32,-3.29597460435593E-17,-3.91886975727153E-17));
#14219=CARTESIAN_POINT('Origin',(0.,0.,0.));
#14220=CARTESIAN_POINT('',(-0.335,0.0149999999999999,-4.10256677714363E-17));
#14221=CARTESIAN_POINT('Origin',(0.22,0.,0.));
#14222=CARTESIAN_POINT('',(-0.22,-6.93889390390723E-18,-2.69422295812418E-17));
#14223=CARTESIAN_POINT('Origin',(0.,0.,0.));
#14224=CARTESIAN_POINT('Origin',(0.,-0.02,0.));
#14225=CARTESIAN_POINT('',(-0.1954,-0.0492,2.39295984553393E-17));
#14226=CARTESIAN_POINT('Origin',(0.,-0.0492,0.));
#14227=CARTESIAN_POINT('',(-0.21,-0.02,-2.57175827820944E-17));
#14228=CARTESIAN_POINT('Origin',(0.,-0.8,0.));
#14229=CARTESIAN_POINT('',(-0.1954,-1.5646,2.39295984553393E-17));
#14230=CARTESIAN_POINT('Origin',(0.,-1.5646,0.));
#14231=CARTESIAN_POINT('',(-0.1954,-0.8,-2.39295984553393E-17));
#14232=CARTESIAN_POINT('Origin',(0.,-1.58,0.));
#14233=CARTESIAN_POINT('',(-0.16,-1.6,-1.95943487863577E-17));
#14234=CARTESIAN_POINT('Origin',(0.,-1.6,0.));
#14235=CARTESIAN_POINT('',(-0.18,-1.58,-2.20436423846524E-17));
#14236=CARTESIAN_POINT('Origin',(0.,-1.6,0.));
#14237=CARTESIAN_POINT('Origin',(0.0866025403784439,-0.4,-0.15));
#14238=CARTESIAN_POINT('',(0.173205080756888,-0.4,0.));
#14239=CARTESIAN_POINT('',(0.0866025403784439,-0.4,-0.15));
#14240=CARTESIAN_POINT('',(0.173205080756888,-0.4,0.));
#14241=CARTESIAN_POINT('',(0.0866025403784439,-0.64,-0.15));
#14242=CARTESIAN_POINT('',(0.0866025403784439,-0.4,-0.15));
#14243=CARTESIAN_POINT('',(0.173205080756888,-0.64,0.));
#14244=CARTESIAN_POINT('',(0.173205080756888,-0.64,0.));
#14245=CARTESIAN_POINT('',(0.173205080756888,-0.4,0.));
#14246=CARTESIAN_POINT('Origin',(-0.0866025403784438,-0.4,-0.15));
#14247=CARTESIAN_POINT('',(-0.0866025403784438,-0.4,-0.15));
#14248=CARTESIAN_POINT('',(0.0866025403784439,-0.4,-0.15));
#14249=CARTESIAN_POINT('',(-0.0866025403784438,-0.64,-0.15));
#14250=CARTESIAN_POINT('',(-0.0866025403784438,-0.4,-0.15));
#14251=CARTESIAN_POINT('',(0.0866025403784439,-0.64,-0.15));
#14252=CARTESIAN_POINT('Origin',(-0.173205080756888,-0.4,-2.77555756156289E-17));
#14253=CARTESIAN_POINT('',(-0.173205080756888,-0.4,-2.12115047744981E-17));
#14254=CARTESIAN_POINT('',(-0.0866025403784438,-0.4,-0.15));
#14255=CARTESIAN_POINT('',(-0.173205080756888,-0.64,-2.77555756156289E-17));
#14256=CARTESIAN_POINT('',(-0.173205080756888,-0.4,-2.12115047744981E-17));
#14257=CARTESIAN_POINT('',(-0.0866025403784438,-0.64,-0.15));
#14258=CARTESIAN_POINT('Origin',(-0.0866025403784439,-0.4,0.15));
#14259=CARTESIAN_POINT('',(-0.0866025403784439,-0.4,0.15));
#14260=CARTESIAN_POINT('',(-0.173205080756888,-0.4,-2.12115047744981E-17));
#14261=CARTESIAN_POINT('',(-0.0866025403784439,-0.64,0.15));
#14262=CARTESIAN_POINT('',(-0.0866025403784439,-0.4,0.15));
#14263=CARTESIAN_POINT('',(-0.173205080756888,-0.64,-2.12115047744981E-17));
#14264=CARTESIAN_POINT('Origin',(0.0866025403784439,-0.4,0.15));
#14265=CARTESIAN_POINT('',(0.0866025403784439,-0.4,0.15));
#14266=CARTESIAN_POINT('',(-0.0866025403784439,-0.4,0.15));
#14267=CARTESIAN_POINT('',(0.0866025403784439,-0.64,0.15));
#14268=CARTESIAN_POINT('',(0.0866025403784439,-0.4,0.15));
#14269=CARTESIAN_POINT('',(-0.0866025403784439,-0.64,0.15));
#14270=CARTESIAN_POINT('Origin',(0.173205080756888,-0.4,0.));
#14271=CARTESIAN_POINT('',(0.0866025403784439,-0.4,0.15));
#14272=CARTESIAN_POINT('',(0.0866025403784439,-0.64,0.15));
#14273=CARTESIAN_POINT('Origin',(0.,-0.4,-2.77555756156289E-17));
#14274=CARTESIAN_POINT('Origin',(0.,-0.64,-2.77555756156289E-17));
#14443=UNCERTAINTY_MEASURE_WITH_UNIT(LENGTH_MEASURE(0.001),#14479,
'DISTANCE_ACCURACY_VALUE',
'Maximum model space distance between geometric entities at asserted c
onnectivities');
#14446=UNCERTAINTY_MEASURE_WITH_UNIT(LENGTH_MEASURE(0.001),#14479,
'DISTANCE_ACCURACY_VALUE',
'Maximum model space distance between geometric entities at asserted c
onnectivities');
#14475=(
GEOMETRIC_REPRESENTATION_CONTEXT(3)
GLOBAL_UNCERTAINTY_ASSIGNED_CONTEXT((#14443))
GLOBAL_UNIT_ASSIGNED_CONTEXT((#14479,#14481,#14482))
REPRESENTATION_CONTEXT('','3D')
);
#14478=(
GEOMETRIC_REPRESENTATION_CONTEXT(3)
GLOBAL_UNCERTAINTY_ASSIGNED_CONTEXT((#14446))
GLOBAL_UNIT_ASSIGNED_CONTEXT((#14479,#14481,#14482))
REPRESENTATION_CONTEXT('','3D')
);
#14479=(
LENGTH_UNIT()
NAMED_UNIT(*)
SI_UNIT(.CENTI.,.METRE.)
);
#14481=(
NAMED_UNIT(*)
PLANE_ANGLE_UNIT()
SI_UNIT($,.RADIAN.)
);
#14482=(
NAMED_UNIT(*)
SI_UNIT($,.STERADIAN.)
SOLID_ANGLE_UNIT()
);
#14511=SHAPE_DEFINITION_REPRESENTATION(#14545,#14631);
#14545=PRODUCT_DEFINITION_SHAPE('',$,#14663);
#14631=SHAPE_REPRESENTATION('',(#9505),#14475);
#14634=PRODUCT_DEFINITION_CONTEXT('part definition',#14729,'design');
#14663=PRODUCT_DEFINITION('Cap Screw - M4x16','Cap Screw - M4x16',#14694,
#14634);
#14694=PRODUCT_DEFINITION_FORMATION('',$,#14759);
#14729=APPLICATION_CONTEXT(
'Core Data for Automotive Mechanical Design Process');
#14730=PRODUCT_CONTEXT('part definition',#14729,'mechanical');
#14759=PRODUCT('Cap Screw - M4x16','Cap Screw - M4x16',
'Cap Screw - M4x16',(#14730));
#14832=COLOUR_RGB('Black',0.12,0.14,0.17);
#14833=FILL_AREA_STYLE_COLOUR('',#14832);
#14834=FILL_AREA_STYLE('',(#14833));
#14835=SURFACE_STYLE_FILL_AREA(#14834);
#14836=SURFACE_SIDE_STYLE('',(#14835));
#14837=SURFACE_STYLE_USAGE(.BOTH.,#14836);
#14838=PRESENTATION_STYLE_ASSIGNMENT((#14837));
ENDSEC;
END-ISO-10303-21;
